ISO-10303-21;
HEADER;
/* Generated by software containing ST-Developer
 * from STEP Tools, Inc. (www.steptools.com) 
 */

FILE_DESCRIPTION(
/* description */ (''),
/* implementation_level */ '2;1');

FILE_NAME(
/* name */ '05_Inner_Bearing_Cup_L68111.step',
/* time_stamp */ '2026-10-25T01:26:34-07:00',
/* author */ (''),
/* organization */ (''),
/* preprocessor_version */ 'ST-DEVELOPER v20.2',
/* originating_system */ 'Autodesk Translation Framework v15.15.0.0',
/* authorisation */ '');

FILE_SCHEMA (('AUTOMOTIVE_DESIGN { 1 0 10303 214 3 1 1 }'));
ENDSEC;

DATA;
#10=MECHANICAL_DESIGN_GEOMETRIC_PRESENTATION_REPRESENTATION('',(#324),#71628);
#298=SHAPE_REPRESENTATION_RELATIONSHIP('SRR','None',#71686,#311);
#311=ADVANCED_BREP_SHAPE_REPRESENTATION('',(#337),#71618);
#324=STYLED_ITEM('',(#71818),#337);
#337=MANIFOLD_SOLID_BREP('Body1',#34211);
#1238=FACE_BOUND('',#6752,.T.);
#1239=FACE_BOUND('',#6757,.T.);
#2595=PLANE('',#36385);
#2596=PLANE('',#36393);
#3060=CYLINDRICAL_SURFACE('',#36381,29.5655);
#4545=FACE_OUTER_BOUND('',#6748,.T.);
#4546=FACE_OUTER_BOUND('',#6749,.T.);
#4547=FACE_OUTER_BOUND('',#6750,.T.);
#4548=FACE_OUTER_BOUND('',#6751,.T.);
#4549=FACE_OUTER_BOUND('',#6753,.T.);
#4550=FACE_OUTER_BOUND('',#6754,.T.);
#4551=FACE_OUTER_BOUND('',#6755,.T.);
#4552=FACE_OUTER_BOUND('',#6756,.T.);
#6748=EDGE_LOOP('',(#28572,#28573,#28574,#28575));
#6749=EDGE_LOOP('',(#28576,#28577,#28578,#28579));
#6750=EDGE_LOOP('',(#28580,#28581,#28582,#28583));
#6751=EDGE_LOOP('',(#28584));
#6752=EDGE_LOOP('',(#28585));
#6753=EDGE_LOOP('',(#28586,#28587,#28588,#28589));
#6754=EDGE_LOOP('',(#28590,#28591,#28592,#28593));
#6755=EDGE_LOOP('',(#28594,#28595,#28596,#28597));
#6756=EDGE_LOOP('',(#28598));
#6757=EDGE_LOOP('',(#28599));
#9929=LINE('',#58020,#12979);
#9930=LINE('',#58025,#12980);
#9931=LINE('',#58029,#12981);
#9932=LINE('',#58035,#12982);
#9933=LINE('',#58039,#12983);
#9934=LINE('',#58043,#12984);
#12979=VECTOR('',#44086,29.1655);
#12980=VECTOR('',#44093,29.5655);
#12981=VECTOR('',#44098,29.2655);
#12982=VECTOR('',#44105,28.3587781164969);
#12983=VECTOR('',#44110,27.3267351683296);
#12984=VECTOR('',#44115,26.6550961100811);
#13960=CIRCLE('',#36379,29.5655);
#13961=CIRCLE('',#36380,28.7655);
#13962=CIRCLE('',#36382,29.5655);
#13963=CIRCLE('',#36384,28.9655);
#13964=CIRCLE('',#36386,28.508778116497);
#13965=CIRCLE('',#36388,28.208778116497);
#13966=CIRCLE('',#36390,26.4446922201623);
#13967=CIRCLE('',#36392,26.8655);
#16363=VERTEX_POINT('',#58017);
#16364=VERTEX_POINT('',#58019);
#16365=VERTEX_POINT('',#58023);
#16366=VERTEX_POINT('',#58027);
#16367=VERTEX_POINT('',#58031);
#16368=VERTEX_POINT('',#58034);
#16369=VERTEX_POINT('',#58038);
#16370=VERTEX_POINT('',#58042);
#20600=EDGE_CURVE('',#16363,#16363,#13960,.T.);
#20601=EDGE_CURVE('',#16363,#16364,#9929,.T.);
#20602=EDGE_CURVE('',#16364,#16364,#13961,.T.);
#20603=EDGE_CURVE('',#16365,#16365,#13962,.T.);
#20604=EDGE_CURVE('',#16365,#16363,#9930,.T.);
#20605=EDGE_CURVE('',#16366,#16366,#13963,.T.);
#20606=EDGE_CURVE('',#16366,#16365,#9931,.T.);
#20607=EDGE_CURVE('',#16367,#16367,#13964,.T.);
#20608=EDGE_CURVE('',#16367,#16368,#9932,.T.);
#20609=EDGE_CURVE('',#16368,#16368,#13965,.T.);
#20610=EDGE_CURVE('',#16368,#16369,#9933,.T.);
#20611=EDGE_CURVE('',#16369,#16369,#13966,.T.);
#20612=EDGE_CURVE('',#16369,#16370,#9934,.T.);
#20613=EDGE_CURVE('',#16370,#16370,#13967,.T.);
#28572=ORIENTED_EDGE('',*,*,#20600,.F.);
#28573=ORIENTED_EDGE('',*,*,#20601,.T.);
#28574=ORIENTED_EDGE('',*,*,#20602,.T.);
#28575=ORIENTED_EDGE('',*,*,#20601,.F.);
#28576=ORIENTED_EDGE('',*,*,#20603,.F.);
#28577=ORIENTED_EDGE('',*,*,#20604,.T.);
#28578=ORIENTED_EDGE('',*,*,#20600,.T.);
#28579=ORIENTED_EDGE('',*,*,#20604,.F.);
#28580=ORIENTED_EDGE('',*,*,#20605,.F.);
#28581=ORIENTED_EDGE('',*,*,#20606,.T.);
#28582=ORIENTED_EDGE('',*,*,#20603,.T.);
#28583=ORIENTED_EDGE('',*,*,#20606,.F.);
#28584=ORIENTED_EDGE('',*,*,#20605,.T.);
#28585=ORIENTED_EDGE('',*,*,#20607,.F.);
#28586=ORIENTED_EDGE('',*,*,#20607,.T.);
#28587=ORIENTED_EDGE('',*,*,#20608,.T.);
#28588=ORIENTED_EDGE('',*,*,#20609,.F.);
#28589=ORIENTED_EDGE('',*,*,#20608,.F.);
#28590=ORIENTED_EDGE('',*,*,#20609,.T.);
#28591=ORIENTED_EDGE('',*,*,#20610,.T.);
#28592=ORIENTED_EDGE('',*,*,#20611,.F.);
#28593=ORIENTED_EDGE('',*,*,#20610,.F.);
#28594=ORIENTED_EDGE('',*,*,#20611,.T.);
#28595=ORIENTED_EDGE('',*,*,#20612,.T.);
#28596=ORIENTED_EDGE('',*,*,#20613,.F.);
#28597=ORIENTED_EDGE('',*,*,#20612,.F.);
#28598=ORIENTED_EDGE('',*,*,#20602,.F.);
#28599=ORIENTED_EDGE('',*,*,#20613,.T.);
#31993=CONICAL_SURFACE('',#36378,29.1655,0.785398163397449);
#31994=CONICAL_SURFACE('',#36383,29.2655,0.78539816339745);
#31995=CONICAL_SURFACE('',#36387,28.358778116497,0.785398163397452);
#31996=CONICAL_SURFACE('',#36389,27.3267351683296,0.157079632679489);
#31997=CONICAL_SURFACE('',#36391,26.6550961100811,0.699606280388882);
#33519=ADVANCED_FACE('',(#4545),#31993,.T.);
#33520=ADVANCED_FACE('',(#4546),#3060,.T.);
#33521=ADVANCED_FACE('',(#4547),#31994,.T.);
#33522=ADVANCED_FACE('',(#4548,#1238),#2595,.T.);
#33523=ADVANCED_FACE('',(#4549),#31995,.F.);
#33524=ADVANCED_FACE('',(#4550),#31996,.F.);
#33525=ADVANCED_FACE('',(#4551),#31997,.F.);
#33526=ADVANCED_FACE('',(#4552,#1239),#2596,.T.);
#34211=CLOSED_SHELL('',(#33519,#33520,#33521,#33522,#33523,#33524,#33525,
#33526));
#36377=AXIS2_PLACEMENT_3D('',#58015,#44080,#44081);
#36378=AXIS2_PLACEMENT_3D('',#58016,#44082,#44083);
#36379=AXIS2_PLACEMENT_3D('',#58018,#44084,#44085);
#36380=AXIS2_PLACEMENT_3D('',#58021,#44087,#44088);
#36381=AXIS2_PLACEMENT_3D('',#58022,#44089,#44090);
#36382=AXIS2_PLACEMENT_3D('',#58024,#44091,#44092);
#36383=AXIS2_PLACEMENT_3D('',#58026,#44094,#44095);
#36384=AXIS2_PLACEMENT_3D('',#58028,#44096,#44097);
#36385=AXIS2_PLACEMENT_3D('',#58030,#44099,#44100);
#36386=AXIS2_PLACEMENT_3D('',#58032,#44101,#44102);
#36387=AXIS2_PLACEMENT_3D('',#58033,#44103,#44104);
#36388=AXIS2_PLACEMENT_3D('',#58036,#44106,#44107);
#36389=AXIS2_PLACEMENT_3D('',#58037,#44108,#44109);
#36390=AXIS2_PLACEMENT_3D('',#58040,#44111,#44112);
#36391=AXIS2_PLACEMENT_3D('',#58041,#44113,#44114);
#36392=AXIS2_PLACEMENT_3D('',#58044,#44116,#44117);
#36393=AXIS2_PLACEMENT_3D('',#58045,#44118,#44119);
#44080=DIRECTION('axis',(0.,0.,1.));
#44081=DIRECTION('refdir',(1.,0.,0.));
#44082=DIRECTION('center_axis',(1.,0.,0.));
#44083=DIRECTION('ref_axis',(0.,1.,0.));
#44084=DIRECTION('center_axis',(1.,0.,0.));
#44085=DIRECTION('ref_axis',(0.,0.,-1.));
#44086=DIRECTION('',(-0.707106781186547,0.707106781186548,8.65956056235494E-17));
#44087=DIRECTION('center_axis',(1.,0.,0.));
#44088=DIRECTION('ref_axis',(0.,0.,-1.));
#44089=DIRECTION('center_axis',(1.,0.,0.));
#44090=DIRECTION('ref_axis',(0.,1.,0.));
#44091=DIRECTION('center_axis',(1.,0.,0.));
#44092=DIRECTION('ref_axis',(0.,0.,-1.));
#44093=DIRECTION('',(-1.,0.,0.));
#44094=DIRECTION('center_axis',(-1.,0.,0.));
#44095=DIRECTION('ref_axis',(0.,1.,0.));
#44096=DIRECTION('center_axis',(1.,0.,0.));
#44097=DIRECTION('ref_axis',(0.,0.,-1.));
#44098=DIRECTION('',(-0.707106781186546,-0.707106781186549,-8.65956056235495E-17));
#44099=DIRECTION('center_axis',(1.,0.,0.));
#44100=DIRECTION('ref_axis',(0.,0.,-1.));
#44101=DIRECTION('center_axis',(1.,0.,0.));
#44102=DIRECTION('ref_axis',(0.,0.,-1.));
#44103=DIRECTION('center_axis',(1.,0.,0.));
#44104=DIRECTION('ref_axis',(0.,1.,0.));
#44105=DIRECTION('',(-0.707106781186545,0.70710678118655,8.65956056235497E-17));
#44106=DIRECTION('center_axis',(1.,0.,0.));
#44107=DIRECTION('ref_axis',(0.,0.,-1.));
#44108=DIRECTION('center_axis',(1.,0.,0.));
#44109=DIRECTION('ref_axis',(0.,1.,0.));
#44110=DIRECTION('',(-0.987688340595138,0.156434465040231,1.91576966887847E-17));
#44111=DIRECTION('center_axis',(1.,0.,0.));
#44112=DIRECTION('ref_axis',(0.,0.,-1.));
#44113=DIRECTION('center_axis',(-1.,0.,0.));
#44114=DIRECTION('ref_axis',(0.,1.,0.));
#44115=DIRECTION('',(-0.765095769134174,-0.643916503945182,-7.88570285474622E-17));
#44116=DIRECTION('center_axis',(1.,0.,0.));
#44117=DIRECTION('ref_axis',(0.,0.,-1.));
#44118=DIRECTION('center_axis',(-1.,0.,0.));
#44119=DIRECTION('ref_axis',(0.,0.,1.));
#58015=CARTESIAN_POINT('',(0.,0.,0.));
#58016=CARTESIAN_POINT('Origin',(0.4,0.,0.));
#58017=CARTESIAN_POINT('',(0.8,-29.5655,-3.62072949401911E-15));
#58018=CARTESIAN_POINT('Origin',(0.8,0.,0.));
#58019=CARTESIAN_POINT('',(-4.85722573273506E-16,-28.7655,-3.52275775008732E-15));
#58020=CARTESIAN_POINT('',(0.4,-29.1655,-3.57174362205321E-15));
#58021=CARTESIAN_POINT('Origin',(0.,0.,0.));
#58022=CARTESIAN_POINT('Origin',(6.069,0.,0.));
#58023=CARTESIAN_POINT('',(11.338,-29.5655,-3.62072949401911E-15));
#58024=CARTESIAN_POINT('Origin',(11.338,0.,0.));
#58025=CARTESIAN_POINT('',(6.069,-29.5655,-3.62072949401911E-15));
#58026=CARTESIAN_POINT('Origin',(11.638,0.,0.));
#58027=CARTESIAN_POINT('',(11.938,-28.9655,-3.54725068607027E-15));
#58028=CARTESIAN_POINT('Origin',(11.938,0.,0.));
#58029=CARTESIAN_POINT('',(11.638,-29.2655,-3.58399009004469E-15));
#58030=CARTESIAN_POINT('Origin',(11.938,28.508778116497,0.));
#58031=CARTESIAN_POINT('',(11.938,-28.508778116497,-3.49131838679701E-15));
#58032=CARTESIAN_POINT('Origin',(11.938,0.,0.));
#58033=CARTESIAN_POINT('Origin',(11.788,0.,0.));
#58034=CARTESIAN_POINT('',(11.638,-28.208778116497,-3.45457898282259E-15));
#58035=CARTESIAN_POINT('',(11.788,-28.358778116497,-3.4729486848098E-15));
#58036=CARTESIAN_POINT('Origin',(11.638,0.,0.));
#58037=CARTESIAN_POINT('Origin',(6.069,0.,0.));
#58038=CARTESIAN_POINT('',(0.5,-26.4446922201623,-3.23854076818586E-15));
#58039=CARTESIAN_POINT('',(6.069,-27.3267351683296,-3.34655987550423E-15));
#58040=CARTESIAN_POINT('Origin',(0.5,0.,0.));
#58041=CARTESIAN_POINT('Origin',(0.25,0.,0.));
#58042=CARTESIAN_POINT('',(-4.85722573273506E-16,-26.8655,-3.29007485824932E-15));
#58043=CARTESIAN_POINT('',(0.25,-26.6550961100811,-3.26430781321759E-15));
#58044=CARTESIAN_POINT('Origin',(0.,0.,0.));
#58045=CARTESIAN_POINT('Origin',(0.,28.7655,0.));
#71603=UNCERTAINTY_MEASURE_WITH_UNIT(LENGTH_MEASURE(0.01),#71629,
'DISTANCE_ACCURACY_VALUE',
'Maximum model space distance between geometric entities at asserted c
onnectivities');
#71613=UNCERTAINTY_MEASURE_WITH_UNIT(LENGTH_MEASURE(0.01),#71629,
'DISTANCE_ACCURACY_VALUE',
'Maximum model space distance between geometric entities at asserted c
onnectivities');
#71618=(
GEOMETRIC_REPRESENTATION_CONTEXT(3)
GLOBAL_UNCERTAINTY_ASSIGNED_CONTEXT((#71603))
GLOBAL_UNIT_ASSIGNED_CONTEXT((#71629,#71631,#71632))
REPRESENTATION_CONTEXT('','3D')
);
#71628=(
GEOMETRIC_REPRESENTATION_CONTEXT(3)
GLOBAL_UNCERTAINTY_ASSIGNED_CONTEXT((#71613))
GLOBAL_UNIT_ASSIGNED_CONTEXT((#71629,#71631,#71632))
REPRESENTATION_CONTEXT('','3D')
);
#71629=(
LENGTH_UNIT()
NAMED_UNIT(*)
SI_UNIT(.MILLI.,.METRE.)
);
#71631=(
NAMED_UNIT(*)
PLANE_ANGLE_UNIT()
SI_UNIT($,.RADIAN.)
);
#71632=(
NAMED_UNIT(*)
SI_UNIT($,.STERADIAN.)
SOLID_ANGLE_UNIT()
);
#71637=SHAPE_DEFINITION_REPRESENTATION(#71651,#71686);
#71651=PRODUCT_DEFINITION_SHAPE('',$,#71701);
#71686=SHAPE_REPRESENTATION('',(#36377),#71618);
#71696=PRODUCT_DEFINITION_CONTEXT('part definition',#71740,'design');
#71701=PRODUCT_DEFINITION('2026-10-25-00-23-51-247',
'05_Inner_Bearing_Cup_L68111',#71715,#71696);
#71715=PRODUCT_DEFINITION_FORMATION('',$,#71746);
#71740=APPLICATION_CONTEXT(
'Core Data for Automotive Mechanical Design Process');
#71741=PRODUCT_CONTEXT('part definition',#71740,'mechanical');
#71746=PRODUCT('2026-10-25-00-23-51-247','05_Inner_Bearing_Cup_L68111',
$,(#71741));
#71812=COLOUR_RGB('Grey',0.48,0.52,0.57);
#71813=FILL_AREA_STYLE_COLOUR('',#71812);
#71814=FILL_AREA_STYLE('',(#71813));
#71815=SURFACE_STYLE_FILL_AREA(#71814);
#71816=SURFACE_SIDE_STYLE('',(#71815));
#71817=SURFACE_STYLE_USAGE(.BOTH.,#71816);
#71818=PRESENTATION_STYLE_ASSIGNMENT((#71817));
ENDSEC;
END-ISO-10303-21;
